ISO-10303-21;
HEADER;
/* Generated by software containing ST-Developer
 * from STEP Tools, Inc. (www.steptools.com) 
 */

FILE_DESCRIPTION(
/* description */ ('Gravity roller conveyor section'),
/* implementation_level */ '2;1');

FILE_NAME(
/* name */ 'M5x40 leg screw.step',
/* time_stamp */ '2026-11-02T07:43:02-08:00',
/* author */ (''),
/* organization */ (''),
/* preprocessor_version */ 'ST-DEVELOPER v20.2',
/* originating_system */ 'Autodesk Translation Framework v15.17.0.0',
/* authorisation */ '');

FILE_SCHEMA (('AUTOMOTIVE_DESIGN { 1 0 10303 214 3 1 1 }'));
ENDSEC;

DATA;
#10=MECHANICAL_DESIGN_GEOMETRIC_PRESENTATION_REPRESENTATION('',(#533),#13821);
#407=CONICAL_SURFACE('',#8244,0.4,0.785398163397448);
#408=CONICAL_SURFACE('',#8248,0.41,0.785398163397448);
#409=CONICAL_SURFACE('',#8252,0.26,0.463647609000806);
#425=ORIENTED_CLOSED_SHELL('',*,#7631,.F.);
#429=BREP_WITH_VOIDS('Body1',#7632,(#425));
#465=SHAPE_REPRESENTATION_RELATIONSHIP('SRR','None',#14002,#499);
#499=ADVANCED_BREP_SHAPE_REPRESENTATION('',(#429),#13789);
#533=STYLED_ITEM('',(#14193),#429);
#629=FACE_BOUND('',#1610,.T.);
#630=FACE_BOUND('',#1618,.T.);
#846=PLANE('',#8228);
#847=PLANE('',#8229);
#848=PLANE('',#8230);
#849=PLANE('',#8231);
#850=PLANE('',#8232);
#851=PLANE('',#8233);
#852=PLANE('',#8234);
#853=PLANE('',#8235);
#854=PLANE('',#8236);
#855=PLANE('',#8241);
#856=PLANE('',#8242);
#857=PLANE('',#8250);
#1162=FACE_OUTER_BOUND('',#1601,.T.);
#1163=FACE_OUTER_BOUND('',#1602,.T.);
#1164=FACE_OUTER_BOUND('',#1603,.T.);
#1165=FACE_OUTER_BOUND('',#1604,.T.);
#1166=FACE_OUTER_BOUND('',#1605,.T.);
#1167=FACE_OUTER_BOUND('',#1606,.T.);
#1168=FACE_OUTER_BOUND('',#1607,.T.);
#1169=FACE_OUTER_BOUND('',#1608,.T.);
#1170=FACE_OUTER_BOUND('',#1609,.T.);
#1171=FACE_OUTER_BOUND('',#1611,.T.);
#1172=FACE_OUTER_BOUND('',#1612,.T.);
#1173=FACE_OUTER_BOUND('',#1613,.T.);
#1174=FACE_OUTER_BOUND('',#1614,.T.);
#1175=FACE_OUTER_BOUND('',#1615,.T.);
#1176=FACE_OUTER_BOUND('',#1616,.T.);
#1177=FACE_OUTER_BOUND('',#1617,.T.);
#1178=FACE_OUTER_BOUND('',#1619,.T.);
#1179=FACE_OUTER_BOUND('',#1620,.T.);
#1601=EDGE_LOOP('',(#6100,#6101,#6102,#6103));
#1602=EDGE_LOOP('',(#6104,#6105,#6106,#6107));
#1603=EDGE_LOOP('',(#6108,#6109,#6110,#6111));
#1604=EDGE_LOOP('',(#6112,#6113,#6114,#6115));
#1605=EDGE_LOOP('',(#6116,#6117,#6118,#6119));
#1606=EDGE_LOOP('',(#6120,#6121,#6122,#6123));
#1607=EDGE_LOOP('',(#6124,#6125,#6126,#6127,#6128,#6129));
#1608=EDGE_LOOP('',(#6130,#6131,#6132,#6133,#6134,#6135));
#1609=EDGE_LOOP('',(#6136));
#1610=EDGE_LOOP('',(#6137));
#1611=EDGE_LOOP('',(#6138,#6139,#6140,#6141));
#1612=EDGE_LOOP('',(#6142));
#1613=EDGE_LOOP('',(#6143));
#1614=EDGE_LOOP('',(#6144,#6145,#6146,#6147));
#1615=EDGE_LOOP('',(#6148,#6149,#6150,#6151));
#1616=EDGE_LOOP('',(#6152,#6153,#6154,#6155));
#1617=EDGE_LOOP('',(#6156));
#1618=EDGE_LOOP('',(#6157));
#1619=EDGE_LOOP('',(#6158,#6159,#6160,#6161));
#1620=EDGE_LOOP('',(#6162,#6163,#6164,#6165));
#2359=LINE('',#12157,#3077);
#2360=LINE('',#12159,#3078);
#2361=LINE('',#12161,#3079);
#2362=LINE('',#12162,#3080);
#2363=LINE('',#12165,#3081);
#2364=LINE('',#12167,#3082);
#2365=LINE('',#12168,#3083);
#2366=LINE('',#12171,#3084);
#2367=LINE('',#12173,#3085);
#2368=LINE('',#12174,#3086);
#2369=LINE('',#12177,#3087);
#2370=LINE('',#12179,#3088);
#2371=LINE('',#12180,#3089);
#2372=LINE('',#12183,#3090);
#2373=LINE('',#12185,#3091);
#2374=LINE('',#12186,#3092);
#2375=LINE('',#12188,#3093);
#2376=LINE('',#12189,#3094);
#2377=LINE('',#12199,#3095);
#2378=LINE('',#12208,#3096);
#2379=LINE('',#12212,#3097);
#2380=LINE('',#12216,#3098);
#2381=LINE('',#12223,#3099);
#2382=LINE('',#12225,#3100);
#3077=VECTOR('',#9600,1.);
#3078=VECTOR('',#9601,1.);
#3079=VECTOR('',#9602,1.);
#3080=VECTOR('',#9603,1.);
#3081=VECTOR('',#9606,1.);
#3082=VECTOR('',#9607,1.);
#3083=VECTOR('',#9608,1.);
#3084=VECTOR('',#9611,1.);
#3085=VECTOR('',#9612,1.);
#3086=VECTOR('',#9613,1.);
#3087=VECTOR('',#9616,1.);
#3088=VECTOR('',#9617,1.);
#3089=VECTOR('',#9618,1.);
#3090=VECTOR('',#9621,1.);
#3091=VECTOR('',#9622,1.);
#3092=VECTOR('',#9623,1.);
#3093=VECTOR('',#9626,1.);
#3094=VECTOR('',#9627,1.);
#3095=VECTOR('',#9640,0.25);
#3096=VECTOR('',#9653,0.4);
#3097=VECTOR('',#9658,0.425);
#3098=VECTOR('',#9663,0.41);
#3099=VECTOR('',#9672,0.26);
#3100=VECTOR('',#9675,0.25);
#3392=CIRCLE('',#8237,0.25);
#3393=CIRCLE('',#8238,0.24505);
#3394=CIRCLE('',#8240,0.25);
#3395=CIRCLE('',#8243,0.375);
#3396=CIRCLE('',#8245,0.425);
#3397=CIRCLE('',#8247,0.425);
#3398=CIRCLE('',#8249,0.395);
#3399=CIRCLE('',#8251,0.27);
#3400=CIRCLE('',#8253,0.24505);
#3890=VERTEX_POINT('',#12155);
#3891=VERTEX_POINT('',#12156);
#3892=VERTEX_POINT('',#12158);
#3893=VERTEX_POINT('',#12160);
#3894=VERTEX_POINT('',#12164);
#3895=VERTEX_POINT('',#12166);
#3896=VERTEX_POINT('',#12170);
#3897=VERTEX_POINT('',#12172);
#3898=VERTEX_POINT('',#12176);
#3899=VERTEX_POINT('',#12178);
#3900=VERTEX_POINT('',#12182);
#3901=VERTEX_POINT('',#12184);
#3902=VERTEX_POINT('',#12193);
#3903=VERTEX_POINT('',#12195);
#3904=VERTEX_POINT('',#12198);
#3905=VERTEX_POINT('',#12203);
#3906=VERTEX_POINT('',#12206);
#3907=VERTEX_POINT('',#12210);
#3908=VERTEX_POINT('',#12214);
#3909=VERTEX_POINT('',#12218);
#3910=VERTEX_POINT('',#12221);
#4687=EDGE_CURVE('',#3890,#3891,#2359,.T.);
#4688=EDGE_CURVE('',#3891,#3892,#2360,.T.);
#4689=EDGE_CURVE('',#3892,#3893,#2361,.T.);
#4690=EDGE_CURVE('',#3890,#3893,#2362,.T.);
#4691=EDGE_CURVE('',#3891,#3894,#2363,.T.);
#4692=EDGE_CURVE('',#3894,#3895,#2364,.T.);
#4693=EDGE_CURVE('',#3895,#3892,#2365,.T.);
#4694=EDGE_CURVE('',#3894,#3896,#2366,.T.);
#4695=EDGE_CURVE('',#3896,#3897,#2367,.T.);
#4696=EDGE_CURVE('',#3897,#3895,#2368,.T.);
#4697=EDGE_CURVE('',#3896,#3898,#2369,.T.);
#4698=EDGE_CURVE('',#3898,#3899,#2370,.T.);
#4699=EDGE_CURVE('',#3899,#3897,#2371,.T.);
#4700=EDGE_CURVE('',#3898,#3900,#2372,.T.);
#4701=EDGE_CURVE('',#3900,#3901,#2373,.T.);
#4702=EDGE_CURVE('',#3901,#3899,#2374,.T.);
#4703=EDGE_CURVE('',#3900,#3890,#2375,.T.);
#4704=EDGE_CURVE('',#3893,#3901,#2376,.T.);
#4705=EDGE_CURVE('',#3902,#3902,#3392,.T.);
#4706=EDGE_CURVE('',#3903,#3903,#3393,.T.);
#4707=EDGE_CURVE('',#3902,#3904,#2377,.T.);
#4708=EDGE_CURVE('',#3904,#3904,#3394,.T.);
#4709=EDGE_CURVE('',#3905,#3905,#3395,.T.);
#4710=EDGE_CURVE('',#3906,#3906,#3396,.T.);
#4711=EDGE_CURVE('',#3906,#3905,#2378,.T.);
#4712=EDGE_CURVE('',#3907,#3907,#3397,.T.);
#4713=EDGE_CURVE('',#3907,#3906,#2379,.T.);
#4714=EDGE_CURVE('',#3908,#3908,#3398,.T.);
#4715=EDGE_CURVE('',#3908,#3907,#2380,.T.);
#4716=EDGE_CURVE('',#3909,#3909,#3399,.T.);
#4717=EDGE_CURVE('',#3910,#3910,#3400,.F.);
#4718=EDGE_CURVE('',#3910,#3909,#2381,.T.);
#4719=EDGE_CURVE('',#3903,#3910,#2382,.T.);
#6100=ORIENTED_EDGE('',*,*,#4687,.T.);
#6101=ORIENTED_EDGE('',*,*,#4688,.T.);
#6102=ORIENTED_EDGE('',*,*,#4689,.T.);
#6103=ORIENTED_EDGE('',*,*,#4690,.F.);
#6104=ORIENTED_EDGE('',*,*,#4691,.T.);
#6105=ORIENTED_EDGE('',*,*,#4692,.T.);
#6106=ORIENTED_EDGE('',*,*,#4693,.T.);
#6107=ORIENTED_EDGE('',*,*,#4688,.F.);
#6108=ORIENTED_EDGE('',*,*,#4694,.T.);
#6109=ORIENTED_EDGE('',*,*,#4695,.T.);
#6110=ORIENTED_EDGE('',*,*,#4696,.T.);
#6111=ORIENTED_EDGE('',*,*,#4692,.F.);
#6112=ORIENTED_EDGE('',*,*,#4697,.T.);
#6113=ORIENTED_EDGE('',*,*,#4698,.T.);
#6114=ORIENTED_EDGE('',*,*,#4699,.T.);
#6115=ORIENTED_EDGE('',*,*,#4695,.F.);
#6116=ORIENTED_EDGE('',*,*,#4700,.T.);
#6117=ORIENTED_EDGE('',*,*,#4701,.T.);
#6118=ORIENTED_EDGE('',*,*,#4702,.T.);
#6119=ORIENTED_EDGE('',*,*,#4698,.F.);
#6120=ORIENTED_EDGE('',*,*,#4703,.T.);
#6121=ORIENTED_EDGE('',*,*,#4690,.T.);
#6122=ORIENTED_EDGE('',*,*,#4704,.T.);
#6123=ORIENTED_EDGE('',*,*,#4701,.F.);
#6124=ORIENTED_EDGE('',*,*,#4703,.F.);
#6125=ORIENTED_EDGE('',*,*,#4700,.F.);
#6126=ORIENTED_EDGE('',*,*,#4697,.F.);
#6127=ORIENTED_EDGE('',*,*,#4694,.F.);
#6128=ORIENTED_EDGE('',*,*,#4691,.F.);
#6129=ORIENTED_EDGE('',*,*,#4687,.F.);
#6130=ORIENTED_EDGE('',*,*,#4704,.F.);
#6131=ORIENTED_EDGE('',*,*,#4689,.F.);
#6132=ORIENTED_EDGE('',*,*,#4693,.F.);
#6133=ORIENTED_EDGE('',*,*,#4696,.F.);
#6134=ORIENTED_EDGE('',*,*,#4699,.F.);
#6135=ORIENTED_EDGE('',*,*,#4702,.F.);
#6136=ORIENTED_EDGE('',*,*,#4705,.T.);
#6137=ORIENTED_EDGE('',*,*,#4706,.F.);
#6138=ORIENTED_EDGE('',*,*,#4705,.F.);
#6139=ORIENTED_EDGE('',*,*,#4707,.T.);
#6140=ORIENTED_EDGE('',*,*,#4708,.T.);
#6141=ORIENTED_EDGE('',*,*,#4707,.F.);
#6142=ORIENTED_EDGE('',*,*,#4708,.F.);
#6143=ORIENTED_EDGE('',*,*,#4709,.F.);
#6144=ORIENTED_EDGE('',*,*,#4710,.F.);
#6145=ORIENTED_EDGE('',*,*,#4711,.T.);
#6146=ORIENTED_EDGE('',*,*,#4709,.T.);
#6147=ORIENTED_EDGE('',*,*,#4711,.F.);
#6148=ORIENTED_EDGE('',*,*,#4712,.F.);
#6149=ORIENTED_EDGE('',*,*,#4713,.T.);
#6150=ORIENTED_EDGE('',*,*,#4710,.T.);
#6151=ORIENTED_EDGE('',*,*,#4713,.F.);
#6152=ORIENTED_EDGE('',*,*,#4714,.F.);
#6153=ORIENTED_EDGE('',*,*,#4715,.T.);
#6154=ORIENTED_EDGE('',*,*,#4712,.T.);
#6155=ORIENTED_EDGE('',*,*,#4715,.F.);
#6156=ORIENTED_EDGE('',*,*,#4714,.T.);
#6157=ORIENTED_EDGE('',*,*,#4716,.F.);
#6158=ORIENTED_EDGE('',*,*,#4717,.F.);
#6159=ORIENTED_EDGE('',*,*,#4718,.T.);
#6160=ORIENTED_EDGE('',*,*,#4716,.T.);
#6161=ORIENTED_EDGE('',*,*,#4718,.F.);
#6162=ORIENTED_EDGE('',*,*,#4706,.T.);
#6163=ORIENTED_EDGE('',*,*,#4719,.T.);
#6164=ORIENTED_EDGE('',*,*,#4717,.T.);
#6165=ORIENTED_EDGE('',*,*,#4719,.F.);
#7141=CYLINDRICAL_SURFACE('',#8239,0.25);
#7142=CYLINDRICAL_SURFACE('',#8246,0.425);
#7143=CYLINDRICAL_SURFACE('',#8254,0.24505);
#7363=ADVANCED_FACE('',(#1162),#846,.F.);
#7364=ADVANCED_FACE('',(#1163),#847,.F.);
#7365=ADVANCED_FACE('',(#1164),#848,.F.);
#7366=ADVANCED_FACE('',(#1165),#849,.F.);
#7367=ADVANCED_FACE('',(#1166),#850,.F.);
#7368=ADVANCED_FACE('',(#1167),#851,.F.);
#7369=ADVANCED_FACE('',(#1168),#852,.F.);
#7370=ADVANCED_FACE('',(#1169),#853,.F.);
#7371=ADVANCED_FACE('',(#1170,#629),#854,.T.);
#7372=ADVANCED_FACE('',(#1171),#7141,.T.);
#7373=ADVANCED_FACE('',(#1172),#855,.F.);
#7374=ADVANCED_FACE('',(#1173),#856,.T.);
#7375=ADVANCED_FACE('',(#1174),#407,.T.);
#7376=ADVANCED_FACE('',(#1175),#7142,.T.);
#7377=ADVANCED_FACE('',(#1176),#408,.T.);
#7378=ADVANCED_FACE('',(#1177,#630),#857,.T.);
#7379=ADVANCED_FACE('',(#1178),#409,.T.);
#7380=ADVANCED_FACE('',(#1179),#7143,.T.);
#7631=CLOSED_SHELL('',(#7363,#7364,#7365,#7366,#7367,#7368,#7369,#7370));
#7632=CLOSED_SHELL('',(#7371,#7372,#7373,#7374,#7375,#7376,#7377,#7378,
#7379,#7380));
#8227=AXIS2_PLACEMENT_3D('',#12153,#9596,#9597);
#8228=AXIS2_PLACEMENT_3D('',#12154,#9598,#9599);
#8229=AXIS2_PLACEMENT_3D('',#12163,#9604,#9605);
#8230=AXIS2_PLACEMENT_3D('',#12169,#9609,#9610);
#8231=AXIS2_PLACEMENT_3D('',#12175,#9614,#9615);
#8232=AXIS2_PLACEMENT_3D('',#12181,#9619,#9620);
#8233=AXIS2_PLACEMENT_3D('',#12187,#9624,#9625);
#8234=AXIS2_PLACEMENT_3D('',#12190,#9628,#9629);
#8235=AXIS2_PLACEMENT_3D('',#12191,#9630,#9631);
#8236=AXIS2_PLACEMENT_3D('',#12192,#9632,#9633);
#8237=AXIS2_PLACEMENT_3D('',#12194,#9634,#9635);
#8238=AXIS2_PLACEMENT_3D('',#12196,#9636,#9637);
#8239=AXIS2_PLACEMENT_3D('',#12197,#9638,#9639);
#8240=AXIS2_PLACEMENT_3D('',#12200,#9641,#9642);
#8241=AXIS2_PLACEMENT_3D('',#12201,#9643,#9644);
#8242=AXIS2_PLACEMENT_3D('',#12202,#9645,#9646);
#8243=AXIS2_PLACEMENT_3D('',#12204,#9647,#9648);
#8244=AXIS2_PLACEMENT_3D('',#12205,#9649,#9650);
#8245=AXIS2_PLACEMENT_3D('',#12207,#9651,#9652);
#8246=AXIS2_PLACEMENT_3D('',#12209,#9654,#9655);
#8247=AXIS2_PLACEMENT_3D('',#12211,#9656,#9657);
#8248=AXIS2_PLACEMENT_3D('',#12213,#9659,#9660);
#8249=AXIS2_PLACEMENT_3D('',#12215,#9661,#9662);
#8250=AXIS2_PLACEMENT_3D('',#12217,#9664,#9665);
#8251=AXIS2_PLACEMENT_3D('',#12219,#9666,#9667);
#8252=AXIS2_PLACEMENT_3D('',#12220,#9668,#9669);
#8253=AXIS2_PLACEMENT_3D('',#12222,#9670,#9671);
#8254=AXIS2_PLACEMENT_3D('',#12224,#9673,#9674);
#9596=DIRECTION('axis',(0.,0.,1.));
#9597=DIRECTION('refdir',(1.,0.,0.));
#9598=DIRECTION('center_axis',(0.866025403784439,0.,-0.5));
#9599=DIRECTION('ref_axis',(0.5,0.,0.866025403784439));
#9600=DIRECTION('',(-0.5,0.,-0.866025403784439));
#9601=DIRECTION('',(0.,-1.,0.));
#9602=DIRECTION('',(0.5,0.,0.866025403784439));
#9603=DIRECTION('',(0.,-1.,0.));
#9604=DIRECTION('center_axis',(1.20185167898973E-16,0.,-1.));
#9605=DIRECTION('ref_axis',(1.,0.,1.20185167898973E-16));
#9606=DIRECTION('',(-1.,0.,-1.20185167898973E-16));
#9607=DIRECTION('',(0.,-1.,0.));
#9608=DIRECTION('',(1.,0.,1.20185167898973E-16));
#9609=DIRECTION('center_axis',(-0.866025403784439,0.,-0.5));
#9610=DIRECTION('ref_axis',(0.5,0.,-0.866025403784439));
#9611=DIRECTION('',(-0.5,0.,0.866025403784439));
#9612=DIRECTION('',(0.,-1.,0.));
#9613=DIRECTION('',(0.5,0.,-0.866025403784439));
#9614=DIRECTION('center_axis',(-0.866025403784439,0.,0.5));
#9615=DIRECTION('ref_axis',(-0.5,0.,-0.866025403784439));
#9616=DIRECTION('',(0.5,0.,0.866025403784439));
#9617=DIRECTION('',(0.,-1.,0.));
#9618=DIRECTION('',(-0.5,0.,-0.866025403784439));
#9619=DIRECTION('center_axis',(-2.40370335797945E-16,0.,1.));
#9620=DIRECTION('ref_axis',(-1.,0.,-2.40370335797945E-16));
#9621=DIRECTION('',(1.,0.,2.40370335797945E-16));
#9622=DIRECTION('',(0.,-1.,0.));
#9623=DIRECTION('',(-1.,0.,-2.40370335797945E-16));
#9624=DIRECTION('center_axis',(0.866025403784439,0.,0.5));
#9625=DIRECTION('ref_axis',(-0.5,0.,0.866025403784439));
#9626=DIRECTION('',(0.5,0.,-0.866025403784439));
#9627=DIRECTION('',(-0.5,0.,0.866025403784439));
#9628=DIRECTION('center_axis',(0.,1.,0.));
#9629=DIRECTION('ref_axis',(1.,0.,0.));
#9630=DIRECTION('center_axis',(0.,-1.,0.));
#9631=DIRECTION('ref_axis',(0.,0.,-1.));
#9632=DIRECTION('center_axis',(0.,1.,0.));
#9633=DIRECTION('ref_axis',(1.,0.,0.));
#9634=DIRECTION('center_axis',(0.,1.,0.));
#9635=DIRECTION('ref_axis',(1.,0.,0.));
#9636=DIRECTION('center_axis',(0.,1.,0.));
#9637=DIRECTION('ref_axis',(1.,0.,0.));
#9638=DIRECTION('center_axis',(0.,1.,0.));
#9639=DIRECTION('ref_axis',(1.,0.,0.));
#9640=DIRECTION('',(0.,-1.,0.));
#9641=DIRECTION('center_axis',(0.,1.,0.));
#9642=DIRECTION('ref_axis',(1.,0.,0.));
#9643=DIRECTION('center_axis',(0.,1.,0.));
#9644=DIRECTION('ref_axis',(1.,0.,0.));
#9645=DIRECTION('center_axis',(0.,1.,0.));
#9646=DIRECTION('ref_axis',(0.,0.,1.));
#9647=DIRECTION('center_axis',(0.,-1.,0.));
#9648=DIRECTION('ref_axis',(1.,0.,0.));
#9649=DIRECTION('center_axis',(0.,-1.,0.));
#9650=DIRECTION('ref_axis',(1.,0.,0.));
#9651=DIRECTION('center_axis',(0.,-1.,0.));
#9652=DIRECTION('ref_axis',(1.,0.,0.));
#9653=DIRECTION('',(0.707106781186548,0.707106781186547,8.65956056235493E-17));
#9654=DIRECTION('center_axis',(0.,-1.,0.));
#9655=DIRECTION('ref_axis',(1.,0.,0.));
#9656=DIRECTION('center_axis',(0.,-1.,0.));
#9657=DIRECTION('ref_axis',(1.,0.,0.));
#9658=DIRECTION('',(0.,1.,0.));
#9659=DIRECTION('center_axis',(0.,1.,0.));
#9660=DIRECTION('ref_axis',(1.,0.,0.));
#9661=DIRECTION('center_axis',(0.,-1.,0.));
#9662=DIRECTION('ref_axis',(1.,0.,0.));
#9663=DIRECTION('',(-0.707106781186547,0.707106781186548,-8.65956056235493E-17));
#9664=DIRECTION('center_axis',(0.,-1.,0.));
#9665=DIRECTION('ref_axis',(0.,0.,-1.));
#9666=DIRECTION('center_axis',(0.,-1.,0.));
#9667=DIRECTION('ref_axis',(1.,0.,0.));
#9668=DIRECTION('center_axis',(0.,1.,0.));
#9669=DIRECTION('ref_axis',(1.,0.,0.));
#9670=DIRECTION('center_axis',(0.,1.,0.));
#9671=DIRECTION('ref_axis',(1.,0.,0.));
#9672=DIRECTION('',(-0.447213595499958,0.894427190999916,-5.47678698264203E-17));
#9673=DIRECTION('center_axis',(0.,-1.,0.));
#9674=DIRECTION('ref_axis',(1.,0.,0.));
#9675=DIRECTION('',(0.,1.,0.));
#12153=CARTESIAN_POINT('',(0.,0.,0.));
#12154=CARTESIAN_POINT('Origin',(0.115470053837925,-0.5,-0.2));
#12155=CARTESIAN_POINT('',(0.23094010767585,-0.5,0.));
#12156=CARTESIAN_POINT('',(0.115470053837925,-0.5,-0.2));
#12157=CARTESIAN_POINT('',(0.23094010767585,-0.5,0.));
#12158=CARTESIAN_POINT('',(0.115470053837925,-0.8,-0.2));
#12159=CARTESIAN_POINT('',(0.115470053837925,-0.5,-0.2));
#12160=CARTESIAN_POINT('',(0.23094010767585,-0.8,0.));
#12161=CARTESIAN_POINT('',(0.23094010767585,-0.8,0.));
#12162=CARTESIAN_POINT('',(0.23094010767585,-0.5,0.));
#12163=CARTESIAN_POINT('Origin',(-0.115470053837925,-0.5,-0.2));
#12164=CARTESIAN_POINT('',(-0.115470053837925,-0.5,-0.2));
#12165=CARTESIAN_POINT('',(0.115470053837925,-0.5,-0.2));
#12166=CARTESIAN_POINT('',(-0.115470053837925,-0.8,-0.2));
#12167=CARTESIAN_POINT('',(-0.115470053837925,-0.5,-0.2));
#12168=CARTESIAN_POINT('',(0.115470053837925,-0.8,-0.2));
#12169=CARTESIAN_POINT('Origin',(-0.23094010767585,-0.5,-2.77555756156289E-17));
#12170=CARTESIAN_POINT('',(-0.23094010767585,-0.5,-2.82820063659975E-17));
#12171=CARTESIAN_POINT('',(-0.115470053837925,-0.5,-0.2));
#12172=CARTESIAN_POINT('',(-0.23094010767585,-0.8,-2.77555756156289E-17));
#12173=CARTESIAN_POINT('',(-0.23094010767585,-0.5,-2.82820063659975E-17));
#12174=CARTESIAN_POINT('',(-0.115470053837925,-0.8,-0.2));
#12175=CARTESIAN_POINT('Origin',(-0.115470053837925,-0.5,0.2));
#12176=CARTESIAN_POINT('',(-0.115470053837925,-0.5,0.2));
#12177=CARTESIAN_POINT('',(-0.23094010767585,-0.5,-2.82820063659975E-17));
#12178=CARTESIAN_POINT('',(-0.115470053837925,-0.8,0.2));
#12179=CARTESIAN_POINT('',(-0.115470053837925,-0.5,0.2));
#12180=CARTESIAN_POINT('',(-0.23094010767585,-0.8,-2.82820063659975E-17));
#12181=CARTESIAN_POINT('Origin',(0.115470053837925,-0.5,0.2));
#12182=CARTESIAN_POINT('',(0.115470053837925,-0.5,0.2));
#12183=CARTESIAN_POINT('',(-0.115470053837925,-0.5,0.2));
#12184=CARTESIAN_POINT('',(0.115470053837925,-0.8,0.2));
#12185=CARTESIAN_POINT('',(0.115470053837925,-0.5,0.2));
#12186=CARTESIAN_POINT('',(-0.115470053837925,-0.8,0.2));
#12187=CARTESIAN_POINT('Origin',(0.23094010767585,-0.5,0.));
#12188=CARTESIAN_POINT('',(0.115470053837925,-0.5,0.2));
#12189=CARTESIAN_POINT('',(0.115470053837925,-0.8,0.2));
#12190=CARTESIAN_POINT('Origin',(0.,-0.5,0.));
#12191=CARTESIAN_POINT('Origin',(0.,-0.8,0.));
#12192=CARTESIAN_POINT('Origin',(0.,-1.9,0.));
#12193=CARTESIAN_POINT('',(-0.25,-1.9,3.06161699786838E-17));
#12194=CARTESIAN_POINT('Origin',(0.,-1.9,0.));
#12195=CARTESIAN_POINT('',(-0.24505,-1.9,3.00099698131059E-17));
#12196=CARTESIAN_POINT('Origin',(0.,-1.9,0.));
#12197=CARTESIAN_POINT('Origin',(0.,-4.,0.));
#12198=CARTESIAN_POINT('',(-0.25,-4.,3.06161699786838E-17));
#12199=CARTESIAN_POINT('',(-0.25,-4.,3.06161699786838E-17));
#12200=CARTESIAN_POINT('Origin',(0.,-4.,0.));
#12201=CARTESIAN_POINT('Origin',(0.,-4.,0.));
#12202=CARTESIAN_POINT('Origin',(0.375,0.5,0.));
#12203=CARTESIAN_POINT('',(-0.375,0.5,-4.59242549680257E-17));
#12204=CARTESIAN_POINT('Origin',(0.,0.5,0.));
#12205=CARTESIAN_POINT('Origin',(0.,0.475,0.));
#12206=CARTESIAN_POINT('',(-0.425,0.45,-5.20474889637625E-17));
#12207=CARTESIAN_POINT('Origin',(0.,0.45,0.));
#12208=CARTESIAN_POINT('',(-0.4,0.475,-4.89858719658941E-17));
#12209=CARTESIAN_POINT('Origin',(0.,0.24,0.));
#12210=CARTESIAN_POINT('',(-0.425,0.0299999999999998,-5.20474889637625E-17));
#12211=CARTESIAN_POINT('Origin',(0.,0.0299999999999998,0.));
#12212=CARTESIAN_POINT('',(-0.425,0.24,-5.20474889637625E-17));
#12213=CARTESIAN_POINT('Origin',(0.,0.0150000000000001,0.));
#12214=CARTESIAN_POINT('',(-0.395,4.85722573273506E-17,-4.83735485663204E-17));
#12215=CARTESIAN_POINT('Origin',(0.,0.,0.));
#12216=CARTESIAN_POINT('',(-0.41,0.0150000000000001,-5.02105187650415E-17));
#12217=CARTESIAN_POINT('Origin',(0.27,0.,0.));
#12218=CARTESIAN_POINT('',(-0.27,0.,-3.30654635769785E-17));
#12219=CARTESIAN_POINT('Origin',(0.,0.,0.));
#12220=CARTESIAN_POINT('Origin',(0.,-0.02,0.));
#12221=CARTESIAN_POINT('',(-0.24505,-0.0498999999999999,3.00099698131059E-17));
#12222=CARTESIAN_POINT('Origin',(0.,-0.0498999999999999,0.));
#12223=CARTESIAN_POINT('',(-0.26,-0.02,-3.18408167778312E-17));
#12224=CARTESIAN_POINT('Origin',(0.,-0.995,0.));
#12225=CARTESIAN_POINT('',(-0.24505,-0.995,-3.00099698131059E-17));
#13750=UNCERTAINTY_MEASURE_WITH_UNIT(LENGTH_MEASURE(0.001),#13822,
'DISTANCE_ACCURACY_VALUE',
'Maximum model space distance between geometric entities at asserted c
onnectivities');
#13782=UNCERTAINTY_MEASURE_WITH_UNIT(LENGTH_MEASURE(0.001),#13822,
'DISTANCE_ACCURACY_VALUE',
'Maximum model space distance between geometric entities at asserted c
onnectivities');
#13789=(
GEOMETRIC_REPRESENTATION_CONTEXT(3)
GLOBAL_UNCERTAINTY_ASSIGNED_CONTEXT((#13750))
GLOBAL_UNIT_ASSIGNED_CONTEXT((#13822,#13824,#13825))
REPRESENTATION_CONTEXT('','3D')
);
#13821=(
GEOMETRIC_REPRESENTATION_CONTEXT(3)
GLOBAL_UNCERTAINTY_ASSIGNED_CONTEXT((#13782))
GLOBAL_UNIT_ASSIGNED_CONTEXT((#13822,#13824,#13825))
REPRESENTATION_CONTEXT('','3D')
);
#13822=(
LENGTH_UNIT()
NAMED_UNIT(*)
SI_UNIT(.CENTI.,.METRE.)
);
#13824=(
NAMED_UNIT(*)
PLANE_ANGLE_UNIT()
SI_UNIT($,.RADIAN.)
);
#13825=(
NAMED_UNIT(*)
SI_UNIT($,.STERADIAN.)
SOLID_ANGLE_UNIT()
);
#13832=SHAPE_DEFINITION_REPRESENTATION(#13870,#14002);
#13870=PRODUCT_DEFINITION_SHAPE('',$,#14041);
#14002=SHAPE_REPRESENTATION('',(#8227),#13789);
#14034=PRODUCT_DEFINITION_CONTEXT('part definition',#14150,'design');
#14041=PRODUCT_DEFINITION('M5x40 leg screw','M5x40 leg screw',#14079,#14034);
#14079=PRODUCT_DEFINITION_FORMATION('',$,#14158);
#14150=APPLICATION_CONTEXT(
'Core Data for Automotive Mechanical Design Process');
#14151=PRODUCT_CONTEXT('part definition',#14150,'mechanical');
#14158=PRODUCT('M5x40 leg screw','M5x40 leg screw','M5x40 leg screw',(#14151));
#14193=PRESENTATION_STYLE_ASSIGNMENT((#14198));
#14198=SURFACE_STYLE_USAGE(.BOTH.,#14203);
#14203=SURFACE_SIDE_STYLE('',(#14208));
#14208=SURFACE_STYLE_FILL_AREA(#14213);
#14213=FILL_AREA_STYLE('CAD Library Painted - Graphite',(#14218));
#14218=FILL_AREA_STYLE_COLOUR('CAD Library Painted - Graphite',#14223);
#14223=COLOUR_RGB('CAD Library Painted - Graphite',0.168627450980392,0.192156862745098,
0.231372549019608);
ENDSEC;
END-ISO-10303-21;
